ISO-10303-21;
HEADER;
/* Generated by software containing ST-Developer
 * from STEP Tools, Inc. (www.steptools.com) 
 */

FILE_DESCRIPTION(
/* description */ (''),
/* implementation_level */ '2;1');

FILE_NAME(
/* name */ 'Pin_02.step',
/* time_stamp */ '2026-10-23T17:00:58+06:00',
/* author */ (''),
/* organization */ (''),
/* preprocessor_version */ 'ST-DEVELOPER v20.2',
/* originating_system */ 'Autodesk Translation Framework v15.15.0.0',
/* authorisation */ '');

FILE_SCHEMA (('AUTOMOTIVE_DESIGN { 1 0 10303 214 3 1 1 }'));
ENDSEC;

DATA;
#10=MECHANICAL_DESIGN_GEOMETRIC_PRESENTATION_REPRESENTATION('',(#117),#11385);
#91=SHAPE_REPRESENTATION_RELATIONSHIP('SRR','None',#11443,#104);
#104=ADVANCED_BREP_SHAPE_REPRESENTATION('',(#130),#11383);
#117=STYLED_ITEM('',(#11567),#130);
#130=MANIFOLD_SOLID_BREP('Pin_02',#5353);
#270=CONICAL_SURFACE('',#6067,0.7,0.785398163397451);
#271=CONICAL_SURFACE('',#6073,0.7,0.785398163397448);
#524=CIRCLE('',#6068,0.649999999999999);
#525=CIRCLE('',#6069,0.75);
#526=CIRCLE('',#6071,0.75);
#527=CIRCLE('',#6074,0.649999999999999);
#602=CYLINDRICAL_SURFACE('',#6070,0.75);
#912=FACE_OUTER_BOUND('',#1277,.T.);
#913=FACE_OUTER_BOUND('',#1278,.T.);
#914=FACE_OUTER_BOUND('',#1279,.T.);
#915=FACE_OUTER_BOUND('',#1280,.T.);
#916=FACE_OUTER_BOUND('',#1281,.T.);
#1277=EDGE_LOOP('',(#4798,#4799,#4800,#4801));
#1278=EDGE_LOOP('',(#4802,#4803,#4804,#4805));
#1279=EDGE_LOOP('',(#4806));
#1280=EDGE_LOOP('',(#4807,#4808,#4809,#4810));
#1281=EDGE_LOOP('',(#4811));
#1736=LINE('',#11272,#2198);
#1737=LINE('',#11276,#2199);
#1738=LINE('',#11281,#2200);
#2198=VECTOR('',#7689,0.699999999999999);
#2199=VECTOR('',#7694,0.75);
#2200=VECTOR('',#7701,0.7);
#2642=VERTEX_POINT('',#11269);
#2643=VERTEX_POINT('',#11271);
#2644=VERTEX_POINT('',#11275);
#2645=VERTEX_POINT('',#11280);
#3364=EDGE_CURVE('',#2642,#2642,#524,.T.);
#3365=EDGE_CURVE('',#2642,#2643,#1736,.T.);
#3366=EDGE_CURVE('',#2643,#2643,#525,.T.);
#3367=EDGE_CURVE('',#2643,#2644,#1737,.T.);
#3368=EDGE_CURVE('',#2644,#2644,#526,.T.);
#3369=EDGE_CURVE('',#2644,#2645,#1738,.T.);
#3370=EDGE_CURVE('',#2645,#2645,#527,.T.);
#4798=ORIENTED_EDGE('',*,*,#3364,.T.);
#4799=ORIENTED_EDGE('',*,*,#3365,.T.);
#4800=ORIENTED_EDGE('',*,*,#3366,.T.);
#4801=ORIENTED_EDGE('',*,*,#3365,.F.);
#4802=ORIENTED_EDGE('',*,*,#3366,.F.);
#4803=ORIENTED_EDGE('',*,*,#3367,.T.);
#4804=ORIENTED_EDGE('',*,*,#3368,.F.);
#4805=ORIENTED_EDGE('',*,*,#3367,.F.);
#4806=ORIENTED_EDGE('',*,*,#3364,.F.);
#4807=ORIENTED_EDGE('',*,*,#3368,.T.);
#4808=ORIENTED_EDGE('',*,*,#3369,.T.);
#4809=ORIENTED_EDGE('',*,*,#3370,.T.);
#4810=ORIENTED_EDGE('',*,*,#3369,.F.);
#4811=ORIENTED_EDGE('',*,*,#3370,.F.);
#5005=PLANE('',#6072);
#5006=PLANE('',#6075);
#5324=ADVANCED_FACE('',(#912),#270,.T.);
#5325=ADVANCED_FACE('',(#913),#602,.T.);
#5326=ADVANCED_FACE('',(#914),#5005,.T.);
#5327=ADVANCED_FACE('',(#915),#271,.T.);
#5328=ADVANCED_FACE('',(#916),#5006,.F.);
#5353=CLOSED_SHELL('',(#5324,#5325,#5326,#5327,#5328));
#6066=AXIS2_PLACEMENT_3D('',#11267,#7683,#7684);
#6067=AXIS2_PLACEMENT_3D('',#11268,#7685,#7686);
#6068=AXIS2_PLACEMENT_3D('',#11270,#7687,#7688);
#6069=AXIS2_PLACEMENT_3D('',#11273,#7690,#7691);
#6070=AXIS2_PLACEMENT_3D('',#11274,#7692,#7693);
#6071=AXIS2_PLACEMENT_3D('',#11277,#7695,#7696);
#6072=AXIS2_PLACEMENT_3D('',#11278,#7697,#7698);
#6073=AXIS2_PLACEMENT_3D('',#11279,#7699,#7700);
#6074=AXIS2_PLACEMENT_3D('',#11282,#7702,#7703);
#6075=AXIS2_PLACEMENT_3D('',#11283,#7704,#7705);
#7683=DIRECTION('axis',(0.,0.,1.));
#7684=DIRECTION('refdir',(1.,0.,0.));
#7685=DIRECTION('center_axis',(-1.,0.,0.));
#7686=DIRECTION('ref_axis',(0.,-1.,-1.22464679914735E-16));
#7687=DIRECTION('center_axis',(-1.,0.,0.));
#7688=DIRECTION('ref_axis',(0.,-1.,-1.22464679914735E-16));
#7689=DIRECTION('',(-0.707106781186546,0.70710678118655,1.73191211247099E-16));
#7690=DIRECTION('center_axis',(1.,0.,0.));
#7691=DIRECTION('ref_axis',(0.,-1.,-1.22464679914735E-16));
#7692=DIRECTION('center_axis',(1.,0.,0.));
#7693=DIRECTION('ref_axis',(0.,-1.,-1.22464679914735E-16));
#7694=DIRECTION('',(-1.,0.,0.));
#7695=DIRECTION('center_axis',(-1.,0.,0.));
#7696=DIRECTION('ref_axis',(0.,-1.,-1.22464679914735E-16));
#7697=DIRECTION('center_axis',(1.,0.,0.));
#7698=DIRECTION('ref_axis',(0.,-1.22464679914735E-16,1.));
#7699=DIRECTION('center_axis',(1.,0.,0.));
#7700=DIRECTION('ref_axis',(0.,-1.,-1.22464679914735E-16));
#7701=DIRECTION('',(-0.707106781186548,-0.707106781186548,-1.73191211247099E-16));
#7702=DIRECTION('center_axis',(1.,0.,0.));
#7703=DIRECTION('ref_axis',(0.,-1.,-1.22464679914735E-16));
#7704=DIRECTION('center_axis',(1.,0.,0.));
#7705=DIRECTION('ref_axis',(0.,-1.22464679914735E-16,1.));
#11267=CARTESIAN_POINT('',(0.,0.,0.));
#11268=CARTESIAN_POINT('Origin',(-2.24952178519528,19.0640879581285,17.6));
#11269=CARTESIAN_POINT('',(-2.19952178519528,19.7140879581285,17.6));
#11270=CARTESIAN_POINT('Origin',(-2.19952178519528,19.0640879581285,17.6));
#11271=CARTESIAN_POINT('',(-2.29952178519528,19.8140879581285,17.6));
#11272=CARTESIAN_POINT('',(-2.24952178519528,19.7640879581285,17.6));
#11273=CARTESIAN_POINT('Origin',(-2.29952178519528,19.0640879581285,17.6));
#11274=CARTESIAN_POINT('Origin',(-7.59952178519528,19.0640879581285,17.6));
#11275=CARTESIAN_POINT('',(-7.49952178519528,19.8140879581285,17.6));
#11276=CARTESIAN_POINT('',(-7.59952178519528,19.8140879581285,17.6));
#11277=CARTESIAN_POINT('Origin',(-7.49952178519528,19.0640879581285,17.6));
#11278=CARTESIAN_POINT('Origin',(-2.19952178519528,19.0640879581285,17.6));
#11279=CARTESIAN_POINT('Origin',(-7.54952178519528,19.0640879581285,17.6));
#11280=CARTESIAN_POINT('',(-7.59952178519528,19.7140879581285,17.6));
#11281=CARTESIAN_POINT('',(-7.54952178519528,19.7640879581285,17.6));
#11282=CARTESIAN_POINT('Origin',(-7.59952178519528,19.0640879581285,17.6));
#11283=CARTESIAN_POINT('Origin',(-7.59952178519528,19.0640879581285,17.6));
#11368=UNCERTAINTY_MEASURE_WITH_UNIT(LENGTH_MEASURE(0.01),#11386,
'DISTANCE_ACCURACY_VALUE',
'Maximum model space distance between geometric entities at asserted c
onnectivities');
#11370=UNCERTAINTY_MEASURE_WITH_UNIT(LENGTH_MEASURE(0.01),#11386,
'DISTANCE_ACCURACY_VALUE',
'Maximum model space distance between geometric entities at asserted c
onnectivities');
#11383=(
GEOMETRIC_REPRESENTATION_CONTEXT(3)
GLOBAL_UNCERTAINTY_ASSIGNED_CONTEXT((#11368))
GLOBAL_UNIT_ASSIGNED_CONTEXT((#11386,#11388,#11389))
REPRESENTATION_CONTEXT('','3D')
);
#11385=(
GEOMETRIC_REPRESENTATION_CONTEXT(3)
GLOBAL_UNCERTAINTY_ASSIGNED_CONTEXT((#11370))
GLOBAL_UNIT_ASSIGNED_CONTEXT((#11386,#11388,#11389))
REPRESENTATION_CONTEXT('','3D')
);
#11386=(
LENGTH_UNIT()
NAMED_UNIT(*)
SI_UNIT(.MILLI.,.METRE.)
);
#11388=(
NAMED_UNIT(*)
PLANE_ANGLE_UNIT()
SI_UNIT($,.RADIAN.)
);
#11389=(
NAMED_UNIT(*)
SI_UNIT($,.STERADIAN.)
SOLID_ANGLE_UNIT()
);
#11402=SHAPE_DEFINITION_REPRESENTATION(#11416,#11443);
#11416=PRODUCT_DEFINITION_SHAPE('',$,#11458);
#11443=SHAPE_REPRESENTATION('',(#6066),#11383);
#11445=PRODUCT_DEFINITION_CONTEXT('part definition',#11489,'design');
#11458=PRODUCT_DEFINITION('Pin_02','Pin_02',#11472,#11445);
#11472=PRODUCT_DEFINITION_FORMATION('',$,#11503);
#11489=APPLICATION_CONTEXT(
'Core Data for Automotive Mechanical Design Process');
#11490=PRODUCT_CONTEXT('part definition',#11489,'mechanical');
#11503=PRODUCT('Pin_02','Pin_02',$,(#11490));
#11561=COLOUR_RGB('Grey',0.48,0.52,0.57);
#11562=FILL_AREA_STYLE_COLOUR('',#11561);
#11563=FILL_AREA_STYLE('',(#11562));
#11564=SURFACE_STYLE_FILL_AREA(#11563);
#11565=SURFACE_SIDE_STYLE('',(#11564));
#11566=SURFACE_STYLE_USAGE(.BOTH.,#11565);
#11567=PRESENTATION_STYLE_ASSIGNMENT((#11566));
ENDSEC;
END-ISO-10303-21;
